ISO-10303-21;
HEADER;
/* Generated by software containing ST-Developer
 * from STEP Tools, Inc. (www.steptools.com) 
 */

FILE_DESCRIPTION(
/* description */ ('V-block with clamp strap'),
/* implementation_level */ '2;1');

FILE_NAME(
/* name */ 'Flat Washer - M5.step',
/* time_stamp */ '2026-10-27T10:50:53-07:00',
/* author */ (''),
/* organization */ (''),
/* preprocessor_version */ 'ST-DEVELOPER v20.2',
/* originating_system */ 'Autodesk Translation Framework v15.17.0.0',
/* authorisation */ '');

FILE_SCHEMA (('AUTOMOTIVE_DESIGN { 1 0 10303 214 3 1 1 }'));
ENDSEC;

DATA;
#10=MECHANICAL_DESIGN_GEOMETRIC_PRESENTATION_REPRESENTATION('',(#277),#7344);
#235=SHAPE_REPRESENTATION_RELATIONSHIP('SRR','None',#7453,#256);
#256=ADVANCED_BREP_SHAPE_REPRESENTATION('',(#296),#7332);
#277=STYLED_ITEM('',(#7638),#296);
#296=MANIFOLD_SOLID_BREP('Body1',#4161);
#357=FACE_BOUND('',#1022,.T.);
#358=FACE_BOUND('',#1024,.T.);
#462=CIRCLE('',#4674,0.265);
#463=CIRCLE('',#4675,0.265);
#464=CIRCLE('',#4677,0.5);
#465=CIRCLE('',#4678,0.5);
#544=CYLINDRICAL_SURFACE('',#4673,0.265);
#545=CYLINDRICAL_SURFACE('',#4676,0.5);
#727=FACE_OUTER_BOUND('',#1019,.T.);
#728=FACE_OUTER_BOUND('',#1020,.T.);
#729=FACE_OUTER_BOUND('',#1021,.T.);
#730=FACE_OUTER_BOUND('',#1023,.T.);
#1019=EDGE_LOOP('',(#3454,#3455,#3456,#3457));
#1020=EDGE_LOOP('',(#3458,#3459,#3460,#3461));
#1021=EDGE_LOOP('',(#3462));
#1022=EDGE_LOOP('',(#3463));
#1023=EDGE_LOOP('',(#3464));
#1024=EDGE_LOOP('',(#3465));
#1402=LINE('',#6886,#1767);
#1403=LINE('',#6892,#1768);
#1767=VECTOR('',#5674,0.265);
#1768=VECTOR('',#5681,0.5);
#2081=VERTEX_POINT('',#6883);
#2082=VERTEX_POINT('',#6885);
#2083=VERTEX_POINT('',#6889);
#2084=VERTEX_POINT('',#6891);
#2553=EDGE_CURVE('',#2081,#2081,#462,.T.);
#2554=EDGE_CURVE('',#2081,#2082,#1402,.T.);
#2555=EDGE_CURVE('',#2082,#2082,#463,.T.);
#2556=EDGE_CURVE('',#2083,#2083,#464,.T.);
#2557=EDGE_CURVE('',#2083,#2084,#1403,.T.);
#2558=EDGE_CURVE('',#2084,#2084,#465,.T.);
#3454=ORIENTED_EDGE('',*,*,#2553,.F.);
#3455=ORIENTED_EDGE('',*,*,#2554,.T.);
#3456=ORIENTED_EDGE('',*,*,#2555,.T.);
#3457=ORIENTED_EDGE('',*,*,#2554,.F.);
#3458=ORIENTED_EDGE('',*,*,#2556,.F.);
#3459=ORIENTED_EDGE('',*,*,#2557,.T.);
#3460=ORIENTED_EDGE('',*,*,#2558,.T.);
#3461=ORIENTED_EDGE('',*,*,#2557,.F.);
#3462=ORIENTED_EDGE('',*,*,#2556,.T.);
#3463=ORIENTED_EDGE('',*,*,#2553,.T.);
#3464=ORIENTED_EDGE('',*,*,#2558,.F.);
#3465=ORIENTED_EDGE('',*,*,#2555,.F.);
#3858=PLANE('',#4679);
#3859=PLANE('',#4680);
#4073=ADVANCED_FACE('',(#727),#544,.F.);
#4074=ADVANCED_FACE('',(#728),#545,.T.);
#4075=ADVANCED_FACE('',(#729,#357),#3858,.T.);
#4076=ADVANCED_FACE('',(#730,#358),#3859,.F.);
#4161=CLOSED_SHELL('',(#4073,#4074,#4075,#4076));
#4672=AXIS2_PLACEMENT_3D('',#6881,#5668,#5669);
#4673=AXIS2_PLACEMENT_3D('',#6882,#5670,#5671);
#4674=AXIS2_PLACEMENT_3D('',#6884,#5672,#5673);
#4675=AXIS2_PLACEMENT_3D('',#6887,#5675,#5676);
#4676=AXIS2_PLACEMENT_3D('',#6888,#5677,#5678);
#4677=AXIS2_PLACEMENT_3D('',#6890,#5679,#5680);
#4678=AXIS2_PLACEMENT_3D('',#6893,#5682,#5683);
#4679=AXIS2_PLACEMENT_3D('',#6894,#5684,#5685);
#4680=AXIS2_PLACEMENT_3D('',#6895,#5686,#5687);
#5668=DIRECTION('axis',(0.,0.,1.));
#5669=DIRECTION('refdir',(1.,0.,0.));
#5670=DIRECTION('center_axis',(0.,1.,0.));
#5671=DIRECTION('ref_axis',(1.,0.,0.));
#5672=DIRECTION('center_axis',(0.,-1.,0.));
#5673=DIRECTION('ref_axis',(1.,0.,0.));
#5674=DIRECTION('',(0.,-1.,0.));
#5675=DIRECTION('center_axis',(0.,-1.,0.));
#5676=DIRECTION('ref_axis',(1.,0.,0.));
#5677=DIRECTION('center_axis',(0.,1.,0.));
#5678=DIRECTION('ref_axis',(1.,0.,0.));
#5679=DIRECTION('center_axis',(0.,1.,0.));
#5680=DIRECTION('ref_axis',(1.,0.,0.));
#5681=DIRECTION('',(0.,-1.,0.));
#5682=DIRECTION('center_axis',(0.,1.,0.));
#5683=DIRECTION('ref_axis',(1.,0.,0.));
#5684=DIRECTION('center_axis',(0.,1.,0.));
#5685=DIRECTION('ref_axis',(1.,0.,0.));
#5686=DIRECTION('center_axis',(0.,1.,0.));
#5687=DIRECTION('ref_axis',(1.,0.,0.));
#6881=CARTESIAN_POINT('',(0.,0.,0.));
#6882=CARTESIAN_POINT('Origin',(0.,0.,0.));
#6883=CARTESIAN_POINT('',(-0.265,0.1,3.24531401774049E-17));
#6884=CARTESIAN_POINT('Origin',(0.,0.1,0.));
#6885=CARTESIAN_POINT('',(-0.265,0.,3.24531401774049E-17));
#6886=CARTESIAN_POINT('',(-0.265,0.,3.24531401774049E-17));
#6887=CARTESIAN_POINT('Origin',(0.,0.,0.));
#6888=CARTESIAN_POINT('Origin',(0.,0.,0.));
#6889=CARTESIAN_POINT('',(-0.5,0.1,6.12323399573677E-17));
#6890=CARTESIAN_POINT('Origin',(0.,0.1,0.));
#6891=CARTESIAN_POINT('',(-0.5,0.,6.12323399573677E-17));
#6892=CARTESIAN_POINT('',(-0.5,0.,6.12323399573677E-17));
#6893=CARTESIAN_POINT('Origin',(0.,0.,0.));
#6894=CARTESIAN_POINT('Origin',(0.,0.1,0.));
#6895=CARTESIAN_POINT('Origin',(0.,0.,0.));
#7306=UNCERTAINTY_MEASURE_WITH_UNIT(LENGTH_MEASURE(0.001),#7345,
'DISTANCE_ACCURACY_VALUE',
'Maximum model space distance between geometric entities at asserted c
onnectivities');
#7318=UNCERTAINTY_MEASURE_WITH_UNIT(LENGTH_MEASURE(0.001),#7345,
'DISTANCE_ACCURACY_VALUE',
'Maximum model space distance between geometric entities at asserted c
onnectivities');
#7332=(
GEOMETRIC_REPRESENTATION_CONTEXT(3)
GLOBAL_UNCERTAINTY_ASSIGNED_CONTEXT((#7306))
GLOBAL_UNIT_ASSIGNED_CONTEXT((#7345,#7347,#7348))
REPRESENTATION_CONTEXT('','3D')
);
#7344=(
GEOMETRIC_REPRESENTATION_CONTEXT(3)
GLOBAL_UNCERTAINTY_ASSIGNED_CONTEXT((#7318))
GLOBAL_UNIT_ASSIGNED_CONTEXT((#7345,#7347,#7348))
REPRESENTATION_CONTEXT('','3D')
);
#7345=(
LENGTH_UNIT()
NAMED_UNIT(*)
SI_UNIT(.CENTI.,.METRE.)
);
#7347=(
NAMED_UNIT(*)
PLANE_ANGLE_UNIT()
SI_UNIT($,.RADIAN.)
);
#7348=(
NAMED_UNIT(*)
SI_UNIT($,.STERADIAN.)
SOLID_ANGLE_UNIT()
);
#7362=SHAPE_DEFINITION_REPRESENTATION(#7387,#7453);
#7387=PRODUCT_DEFINITION_SHAPE('',$,#7479);
#7453=SHAPE_REPRESENTATION('',(#4672),#7332);
#7465=PRODUCT_DEFINITION_CONTEXT('part definition',#7542,'design');
#7479=PRODUCT_DEFINITION('Flat Washer - M5','Flat Washer - M5',#7504,#7465);
#7504=PRODUCT_DEFINITION_FORMATION('',$,#7557);
#7542=APPLICATION_CONTEXT(
'Core Data for Automotive Mechanical Design Process');
#7543=PRODUCT_CONTEXT('part definition',#7542,'mechanical');
#7557=PRODUCT('Flat Washer - M5','Flat Washer - M5','Flat Washer - M5',
(#7543));
#7632=COLOUR_RGB('Black',0.12,0.14,0.17);
#7633=FILL_AREA_STYLE_COLOUR('',#7632);
#7634=FILL_AREA_STYLE('',(#7633));
#7635=SURFACE_STYLE_FILL_AREA(#7634);
#7636=SURFACE_SIDE_STYLE('',(#7635));
#7637=SURFACE_STYLE_USAGE(.BOTH.,#7636);
#7638=PRESENTATION_STYLE_ASSIGNMENT((#7637));
ENDSEC;
END-ISO-10303-21;
